ISO-10303-21;
HEADER;
/* Generated by software containing ST-Developer
 * from STEP Tools, Inc. (www.steptools.com) 
 */

FILE_DESCRIPTION(
/* description */ ('Bell-crank linkage with push rods'),
/* implementation_level */ '2;1');

FILE_NAME(
/* name */ 'M4x4 collar screw.step',
/* time_stamp */ '2026-10-28T03:25:15-07:00',
/* author */ (''),
/* organization */ (''),
/* preprocessor_version */ 'ST-DEVELOPER v20.2',
/* originating_system */ 'Autodesk Translation Framework v15.17.0.0',
/* authorisation */ '');

FILE_SCHEMA (('AUTOMOTIVE_DESIGN { 1 0 10303 214 3 1 1 }'));
ENDSEC;

DATA;
#10=MECHANICAL_DESIGN_GEOMETRIC_PRESENTATION_REPRESENTATION('',(#642),#16678);
#447=CONICAL_SURFACE('',#10153,0.185,0.785398163397449);
#526=SHAPE_REPRESENTATION_RELATIONSHIP('SRR','None',#16944,#580);
#580=ADVANCED_BREP_SHAPE_REPRESENTATION('',(#702),#16649);
#642=STYLED_ITEM('',(#17298),#702);
#702=MANIFOLD_SOLID_BREP('Body1',#8834);
#857=FACE_BOUND('',#2236,.T.);
#1134=PLANE('',#10142);
#1135=PLANE('',#10144);
#1136=PLANE('',#10145);
#1137=PLANE('',#10146);
#1138=PLANE('',#10147);
#1139=PLANE('',#10148);
#1140=PLANE('',#10149);
#1141=PLANE('',#10150);
#1142=PLANE('',#10151);
#1573=FACE_OUTER_BOUND('',#2227,.T.);
#1574=FACE_OUTER_BOUND('',#2228,.T.);
#1575=FACE_OUTER_BOUND('',#2229,.T.);
#1576=FACE_OUTER_BOUND('',#2230,.T.);
#1577=FACE_OUTER_BOUND('',#2231,.T.);
#1578=FACE_OUTER_BOUND('',#2232,.T.);
#1579=FACE_OUTER_BOUND('',#2233,.T.);
#1580=FACE_OUTER_BOUND('',#2234,.T.);
#1581=FACE_OUTER_BOUND('',#2235,.T.);
#1582=FACE_OUTER_BOUND('',#2237,.T.);
#1583=FACE_OUTER_BOUND('',#2238,.T.);
#2227=EDGE_LOOP('',(#7289));
#2228=EDGE_LOOP('',(#7290,#7291,#7292,#7293));
#2229=EDGE_LOOP('',(#7294,#7295,#7296,#7297));
#2230=EDGE_LOOP('',(#7298,#7299,#7300,#7301));
#2231=EDGE_LOOP('',(#7302,#7303,#7304,#7305));
#2232=EDGE_LOOP('',(#7306,#7307,#7308,#7309));
#2233=EDGE_LOOP('',(#7310,#7311,#7312,#7313));
#2234=EDGE_LOOP('',(#7314,#7315,#7316,#7317,#7318,#7319));
#2235=EDGE_LOOP('',(#7320));
#2236=EDGE_LOOP('',(#7321,#7322,#7323,#7324,#7325,#7326));
#2237=EDGE_LOOP('',(#7327,#7328,#7329,#7330));
#2238=EDGE_LOOP('',(#7331,#7332,#7333,#7334));
#2860=LINE('',#15590,#3409);
#2861=LINE('',#15592,#3410);
#2862=LINE('',#15594,#3411);
#2863=LINE('',#15595,#3412);
#2864=LINE('',#15598,#3413);
#2865=LINE('',#15600,#3414);
#2866=LINE('',#15601,#3415);
#2867=LINE('',#15604,#3416);
#2868=LINE('',#15606,#3417);
#2869=LINE('',#15607,#3418);
#2870=LINE('',#15610,#3419);
#2871=LINE('',#15612,#3420);
#2872=LINE('',#15613,#3421);
#2873=LINE('',#15616,#3422);
#2874=LINE('',#15618,#3423);
#2875=LINE('',#15619,#3424);
#2876=LINE('',#15621,#3425);
#2877=LINE('',#15622,#3426);
#2878=LINE('',#15630,#3427);
#2879=LINE('',#15632,#3428);
#3409=VECTOR('',#12340,1.);
#3410=VECTOR('',#12341,1.);
#3411=VECTOR('',#12342,1.);
#3412=VECTOR('',#12343,1.);
#3413=VECTOR('',#12346,1.);
#3414=VECTOR('',#12347,1.);
#3415=VECTOR('',#12348,1.);
#3416=VECTOR('',#12351,1.);
#3417=VECTOR('',#12352,1.);
#3418=VECTOR('',#12353,1.);
#3419=VECTOR('',#12356,1.);
#3420=VECTOR('',#12357,1.);
#3421=VECTOR('',#12358,1.);
#3422=VECTOR('',#12361,1.);
#3423=VECTOR('',#12362,1.);
#3424=VECTOR('',#12363,1.);
#3425=VECTOR('',#12366,1.);
#3426=VECTOR('',#12367,1.);
#3427=VECTOR('',#12378,0.185);
#3428=VECTOR('',#12381,0.2);
#3952=CIRCLE('',#10143,0.1954);
#3953=CIRCLE('',#10152,0.17);
#3954=CIRCLE('',#10154,0.1954);
#4575=VERTEX_POINT('',#15585);
#4576=VERTEX_POINT('',#15588);
#4577=VERTEX_POINT('',#15589);
#4578=VERTEX_POINT('',#15591);
#4579=VERTEX_POINT('',#15593);
#4580=VERTEX_POINT('',#15597);
#4581=VERTEX_POINT('',#15599);
#4582=VERTEX_POINT('',#15603);
#4583=VERTEX_POINT('',#15605);
#4584=VERTEX_POINT('',#15609);
#4585=VERTEX_POINT('',#15611);
#4586=VERTEX_POINT('',#15615);
#4587=VERTEX_POINT('',#15617);
#4588=VERTEX_POINT('',#15625);
#4589=VERTEX_POINT('',#15628);
#5522=EDGE_CURVE('',#4575,#4575,#3952,.T.);
#5523=EDGE_CURVE('',#4576,#4577,#2860,.T.);
#5524=EDGE_CURVE('',#4576,#4578,#2861,.T.);
#5525=EDGE_CURVE('',#4578,#4579,#2862,.T.);
#5526=EDGE_CURVE('',#4577,#4579,#2863,.T.);
#5527=EDGE_CURVE('',#4580,#4576,#2864,.T.);
#5528=EDGE_CURVE('',#4580,#4581,#2865,.T.);
#5529=EDGE_CURVE('',#4581,#4578,#2866,.T.);
#5530=EDGE_CURVE('',#4582,#4580,#2867,.T.);
#5531=EDGE_CURVE('',#4582,#4583,#2868,.T.);
#5532=EDGE_CURVE('',#4583,#4581,#2869,.T.);
#5533=EDGE_CURVE('',#4584,#4582,#2870,.T.);
#5534=EDGE_CURVE('',#4584,#4585,#2871,.T.);
#5535=EDGE_CURVE('',#4585,#4583,#2872,.T.);
#5536=EDGE_CURVE('',#4586,#4584,#2873,.T.);
#5537=EDGE_CURVE('',#4586,#4587,#2874,.T.);
#5538=EDGE_CURVE('',#4587,#4585,#2875,.T.);
#5539=EDGE_CURVE('',#4577,#4586,#2876,.T.);
#5540=EDGE_CURVE('',#4579,#4587,#2877,.T.);
#5541=EDGE_CURVE('',#4588,#4588,#3953,.T.);
#5542=EDGE_CURVE('',#4589,#4589,#3954,.T.);
#5543=EDGE_CURVE('',#4589,#4588,#2878,.T.);
#5544=EDGE_CURVE('',#4575,#4589,#2879,.T.);
#7289=ORIENTED_EDGE('',*,*,#5522,.F.);
#7290=ORIENTED_EDGE('',*,*,#5523,.F.);
#7291=ORIENTED_EDGE('',*,*,#5524,.T.);
#7292=ORIENTED_EDGE('',*,*,#5525,.T.);
#7293=ORIENTED_EDGE('',*,*,#5526,.F.);
#7294=ORIENTED_EDGE('',*,*,#5527,.F.);
#7295=ORIENTED_EDGE('',*,*,#5528,.T.);
#7296=ORIENTED_EDGE('',*,*,#5529,.T.);
#7297=ORIENTED_EDGE('',*,*,#5524,.F.);
#7298=ORIENTED_EDGE('',*,*,#5530,.F.);
#7299=ORIENTED_EDGE('',*,*,#5531,.T.);
#7300=ORIENTED_EDGE('',*,*,#5532,.T.);
#7301=ORIENTED_EDGE('',*,*,#5528,.F.);
#7302=ORIENTED_EDGE('',*,*,#5533,.F.);
#7303=ORIENTED_EDGE('',*,*,#5534,.T.);
#7304=ORIENTED_EDGE('',*,*,#5535,.T.);
#7305=ORIENTED_EDGE('',*,*,#5531,.F.);
#7306=ORIENTED_EDGE('',*,*,#5536,.F.);
#7307=ORIENTED_EDGE('',*,*,#5537,.T.);
#7308=ORIENTED_EDGE('',*,*,#5538,.T.);
#7309=ORIENTED_EDGE('',*,*,#5534,.F.);
#7310=ORIENTED_EDGE('',*,*,#5539,.F.);
#7311=ORIENTED_EDGE('',*,*,#5526,.T.);
#7312=ORIENTED_EDGE('',*,*,#5540,.T.);
#7313=ORIENTED_EDGE('',*,*,#5537,.F.);
#7314=ORIENTED_EDGE('',*,*,#5540,.F.);
#7315=ORIENTED_EDGE('',*,*,#5525,.F.);
#7316=ORIENTED_EDGE('',*,*,#5529,.F.);
#7317=ORIENTED_EDGE('',*,*,#5532,.F.);
#7318=ORIENTED_EDGE('',*,*,#5535,.F.);
#7319=ORIENTED_EDGE('',*,*,#5538,.F.);
#7320=ORIENTED_EDGE('',*,*,#5541,.F.);
#7321=ORIENTED_EDGE('',*,*,#5523,.T.);
#7322=ORIENTED_EDGE('',*,*,#5539,.T.);
#7323=ORIENTED_EDGE('',*,*,#5536,.T.);
#7324=ORIENTED_EDGE('',*,*,#5533,.T.);
#7325=ORIENTED_EDGE('',*,*,#5530,.T.);
#7326=ORIENTED_EDGE('',*,*,#5527,.T.);
#7327=ORIENTED_EDGE('',*,*,#5542,.F.);
#7328=ORIENTED_EDGE('',*,*,#5543,.T.);
#7329=ORIENTED_EDGE('',*,*,#5541,.T.);
#7330=ORIENTED_EDGE('',*,*,#5543,.F.);
#7331=ORIENTED_EDGE('',*,*,#5522,.T.);
#7332=ORIENTED_EDGE('',*,*,#5544,.T.);
#7333=ORIENTED_EDGE('',*,*,#5542,.T.);
#7334=ORIENTED_EDGE('',*,*,#5544,.F.);
#8193=CYLINDRICAL_SURFACE('',#10155,0.1954);
#8598=ADVANCED_FACE('',(#1573),#1134,.F.);
#8599=ADVANCED_FACE('',(#1574),#1135,.F.);
#8600=ADVANCED_FACE('',(#1575),#1136,.F.);
#8601=ADVANCED_FACE('',(#1576),#1137,.F.);
#8602=ADVANCED_FACE('',(#1577),#1138,.F.);
#8603=ADVANCED_FACE('',(#1578),#1139,.F.);
#8604=ADVANCED_FACE('',(#1579),#1140,.F.);
#8605=ADVANCED_FACE('',(#1580),#1141,.F.);
#8606=ADVANCED_FACE('',(#1581,#857),#1142,.T.);
#8607=ADVANCED_FACE('',(#1582),#447,.T.);
#8608=ADVANCED_FACE('',(#1583),#8193,.T.);
#8834=CLOSED_SHELL('',(#8598,#8599,#8600,#8601,#8602,#8603,#8604,#8605,
#8606,#8607,#8608));
#10141=AXIS2_PLACEMENT_3D('',#15583,#12332,#12333);
#10142=AXIS2_PLACEMENT_3D('',#15584,#12334,#12335);
#10143=AXIS2_PLACEMENT_3D('',#15586,#12336,#12337);
#10144=AXIS2_PLACEMENT_3D('',#15587,#12338,#12339);
#10145=AXIS2_PLACEMENT_3D('',#15596,#12344,#12345);
#10146=AXIS2_PLACEMENT_3D('',#15602,#12349,#12350);
#10147=AXIS2_PLACEMENT_3D('',#15608,#12354,#12355);
#10148=AXIS2_PLACEMENT_3D('',#15614,#12359,#12360);
#10149=AXIS2_PLACEMENT_3D('',#15620,#12364,#12365);
#10150=AXIS2_PLACEMENT_3D('',#15623,#12368,#12369);
#10151=AXIS2_PLACEMENT_3D('',#15624,#12370,#12371);
#10152=AXIS2_PLACEMENT_3D('',#15626,#12372,#12373);
#10153=AXIS2_PLACEMENT_3D('',#15627,#12374,#12375);
#10154=AXIS2_PLACEMENT_3D('',#15629,#12376,#12377);
#10155=AXIS2_PLACEMENT_3D('',#15631,#12379,#12380);
#12332=DIRECTION('axis',(0.,0.,1.));
#12333=DIRECTION('refdir',(1.,0.,0.));
#12334=DIRECTION('center_axis',(0.,1.,0.));
#12335=DIRECTION('ref_axis',(1.,0.,0.));
#12336=DIRECTION('center_axis',(0.,1.,0.));
#12337=DIRECTION('ref_axis',(1.,0.,0.));
#12338=DIRECTION('center_axis',(0.866025403784439,0.,-0.5));
#12339=DIRECTION('ref_axis',(0.5,0.,0.866025403784439));
#12340=DIRECTION('',(0.5,0.,0.866025403784439));
#12341=DIRECTION('',(0.,-1.,0.));
#12342=DIRECTION('',(0.5,0.,0.866025403784439));
#12343=DIRECTION('',(0.,-1.,0.));
#12344=DIRECTION('center_axis',(1.20185167898973E-16,0.,-1.));
#12345=DIRECTION('ref_axis',(1.,0.,1.20185167898973E-16));
#12346=DIRECTION('',(1.,0.,1.20185167898973E-16));
#12347=DIRECTION('',(0.,-1.,0.));
#12348=DIRECTION('',(1.,0.,1.20185167898973E-16));
#12349=DIRECTION('center_axis',(-0.866025403784439,0.,-0.5));
#12350=DIRECTION('ref_axis',(0.5,0.,-0.866025403784439));
#12351=DIRECTION('',(0.5,0.,-0.866025403784439));
#12352=DIRECTION('',(0.,-1.,0.));
#12353=DIRECTION('',(0.5,0.,-0.866025403784439));
#12354=DIRECTION('center_axis',(-0.866025403784439,0.,0.5));
#12355=DIRECTION('ref_axis',(-0.5,0.,-0.866025403784439));
#12356=DIRECTION('',(-0.5,0.,-0.866025403784439));
#12357=DIRECTION('',(0.,-1.,0.));
#12358=DIRECTION('',(-0.5,0.,-0.866025403784439));
#12359=DIRECTION('center_axis',(-2.40370335797945E-16,0.,1.));
#12360=DIRECTION('ref_axis',(-1.,0.,-2.40370335797945E-16));
#12361=DIRECTION('',(-1.,0.,-2.40370335797945E-16));
#12362=DIRECTION('',(0.,-1.,0.));
#12363=DIRECTION('',(-1.,0.,-2.40370335797945E-16));
#12364=DIRECTION('center_axis',(0.866025403784439,0.,0.5));
#12365=DIRECTION('ref_axis',(-0.5,0.,0.866025403784439));
#12366=DIRECTION('',(-0.5,0.,0.866025403784439));
#12367=DIRECTION('',(-0.5,0.,0.866025403784439));
#12368=DIRECTION('center_axis',(0.,-1.,0.));
#12369=DIRECTION('ref_axis',(0.,0.,-1.));
#12370=DIRECTION('center_axis',(0.,1.,0.));
#12371=DIRECTION('ref_axis',(0.,0.,1.));
#12372=DIRECTION('center_axis',(0.,-1.,0.));
#12373=DIRECTION('ref_axis',(1.,0.,0.));
#12374=DIRECTION('center_axis',(0.,-1.,0.));
#12375=DIRECTION('ref_axis',(1.,0.,0.));
#12376=DIRECTION('center_axis',(0.,-1.,0.));
#12377=DIRECTION('ref_axis',(1.,0.,0.));
#12378=DIRECTION('',(0.707106781186548,0.707106781186547,8.65956056235494E-17));
#12379=DIRECTION('center_axis',(0.,-1.,0.));
#12380=DIRECTION('ref_axis',(1.,0.,0.));
#12381=DIRECTION('',(0.,1.,0.));
#15583=CARTESIAN_POINT('',(0.,0.,0.));
#15584=CARTESIAN_POINT('Origin',(0.,-0.4,0.));
#15585=CARTESIAN_POINT('',(-0.1954,-0.4,2.39295984553393E-17));
#15586=CARTESIAN_POINT('Origin',(0.,-0.4,0.));
#15587=CARTESIAN_POINT('Origin',(0.0577350269189626,0.,-0.1));
#15588=CARTESIAN_POINT('',(0.0577350269189626,0.,-0.1));
#15589=CARTESIAN_POINT('',(0.115470053837925,0.,0.));
#15590=CARTESIAN_POINT('',(0.0934187836487032,0.,-0.0381939203391614));
#15591=CARTESIAN_POINT('',(0.0577350269189626,-0.2,-0.1));
#15592=CARTESIAN_POINT('',(0.0577350269189626,0.,-0.1));
#15593=CARTESIAN_POINT('',(0.115470053837925,-0.2,0.));
#15594=CARTESIAN_POINT('',(0.115470053837925,-0.2,0.));
#15595=CARTESIAN_POINT('',(0.115470053837925,0.,0.));
#15596=CARTESIAN_POINT('Origin',(-0.0577350269189626,0.,-0.1));
#15597=CARTESIAN_POINT('',(-0.0577350269189626,0.,-0.1));
#15598=CARTESIAN_POINT('',(0.0561324865405187,0.,-0.1));
#15599=CARTESIAN_POINT('',(-0.0577350269189626,-0.2,-0.1));
#15600=CARTESIAN_POINT('',(-0.0577350269189626,0.,-0.1));
#15601=CARTESIAN_POINT('',(0.0577350269189626,-0.2,-0.1));
#15602=CARTESIAN_POINT('Origin',(-0.115470053837925,0.,-1.38777878078145E-17));
#15603=CARTESIAN_POINT('',(-0.115470053837925,0.,-1.41410031829988E-17));
#15604=CARTESIAN_POINT('',(-0.0797862971081845,0.,-0.0618060796608387));
#15605=CARTESIAN_POINT('',(-0.115470053837925,-0.2,-1.38777878078145E-17));
#15606=CARTESIAN_POINT('',(-0.115470053837925,0.,-1.41410031829988E-17));
#15607=CARTESIAN_POINT('',(-0.0577350269189626,-0.2,-0.1));
#15608=CARTESIAN_POINT('Origin',(-0.0577350269189626,0.,0.1));
#15609=CARTESIAN_POINT('',(-0.0577350269189626,0.,0.1));
#15610=CARTESIAN_POINT('',(-0.0509187836487033,0.,0.111806079660839));
#15611=CARTESIAN_POINT('',(-0.0577350269189626,-0.2,0.1));
#15612=CARTESIAN_POINT('',(-0.0577350269189626,0.,0.1));
#15613=CARTESIAN_POINT('',(-0.115470053837925,-0.2,-1.41410031829988E-17));
#15614=CARTESIAN_POINT('Origin',(0.0577350269189626,0.,0.1));
#15615=CARTESIAN_POINT('',(0.0577350269189626,0.,0.1));
#15616=CARTESIAN_POINT('',(0.113867513459481,0.,0.1));
#15617=CARTESIAN_POINT('',(0.0577350269189626,-0.2,0.1));
#15618=CARTESIAN_POINT('',(0.0577350269189626,0.,0.1));
#15619=CARTESIAN_POINT('',(-0.0577350269189626,-0.2,0.1));
#15620=CARTESIAN_POINT('Origin',(0.115470053837925,0.,0.));
#15621=CARTESIAN_POINT('',(0.122286297108185,0.,-0.0118060796608386));
#15622=CARTESIAN_POINT('',(0.0577350269189626,-0.2,0.1));
#15623=CARTESIAN_POINT('Origin',(0.,-0.2,0.));
#15624=CARTESIAN_POINT('Origin',(0.17,0.,0.));
#15625=CARTESIAN_POINT('',(-0.17,-8.67361737988404E-18,-2.0818995585505E-17));
#15626=CARTESIAN_POINT('Origin',(0.,0.,0.));
#15627=CARTESIAN_POINT('Origin',(0.,-0.015,0.));
#15628=CARTESIAN_POINT('',(-0.1954,-0.0254,-2.39295984553393E-17));
#15629=CARTESIAN_POINT('Origin',(0.,-0.0254,0.));
#15630=CARTESIAN_POINT('',(-0.185,-0.015,-2.2655965784226E-17));
#15631=CARTESIAN_POINT('Origin',(0.,-0.2775,0.));
#15632=CARTESIAN_POINT('',(-0.1954,-0.2775,-2.39295984553393E-17));
#16585=UNCERTAINTY_MEASURE_WITH_UNIT(LENGTH_MEASURE(0.001),#16679,
'DISTANCE_ACCURACY_VALUE',
'Maximum model space distance between geometric entities at asserted c
onnectivities');
#16614=UNCERTAINTY_MEASURE_WITH_UNIT(LENGTH_MEASURE(0.001),#16679,
'DISTANCE_ACCURACY_VALUE',
'Maximum model space distance between geometric entities at asserted c
onnectivities');
#16649=(
GEOMETRIC_REPRESENTATION_CONTEXT(3)
GLOBAL_UNCERTAINTY_ASSIGNED_CONTEXT((#16585))
GLOBAL_UNIT_ASSIGNED_CONTEXT((#16679,#16681,#16682))
REPRESENTATION_CONTEXT('','3D')
);
#16678=(
GEOMETRIC_REPRESENTATION_CONTEXT(3)
GLOBAL_UNCERTAINTY_ASSIGNED_CONTEXT((#16614))
GLOBAL_UNIT_ASSIGNED_CONTEXT((#16679,#16681,#16682))
REPRESENTATION_CONTEXT('','3D')
);
#16679=(
LENGTH_UNIT()
NAMED_UNIT(*)
SI_UNIT(.CENTI.,.METRE.)
);
#16681=(
NAMED_UNIT(*)
PLANE_ANGLE_UNIT()
SI_UNIT($,.RADIAN.)
);
#16682=(
NAMED_UNIT(*)
SI_UNIT($,.STERADIAN.)
SOLID_ANGLE_UNIT()
);
#16717=SHAPE_DEFINITION_REPRESENTATION(#16785,#16944);
#16785=PRODUCT_DEFINITION_SHAPE('',$,#17008);
#16944=SHAPE_REPRESENTATION('',(#10141),#16649);
#16973=PRODUCT_DEFINITION_CONTEXT('part definition',#17164,'design');
#17008=PRODUCT_DEFINITION('M4x4 collar screw','M4x4 collar screw',#17071,
#16973);
#17071=PRODUCT_DEFINITION_FORMATION('',$,#17200);
#17164=APPLICATION_CONTEXT(
'Core Data for Automotive Mechanical Design Process');
#17165=PRODUCT_CONTEXT('part definition',#17164,'mechanical');
#17200=PRODUCT('M4x4 collar screw','M4x4 collar screw',
'M4x4 collar screw',(#17165));
#17292=COLOUR_RGB('Black',0.12,0.14,0.17);
#17293=FILL_AREA_STYLE_COLOUR('',#17292);
#17294=FILL_AREA_STYLE('',(#17293));
#17295=SURFACE_STYLE_FILL_AREA(#17294);
#17296=SURFACE_SIDE_STYLE('',(#17295));
#17297=SURFACE_STYLE_USAGE(.BOTH.,#17296);
#17298=PRESENTATION_STYLE_ASSIGNMENT((#17297));
ENDSEC;
END-ISO-10303-21;
